ISO-10303-21;
HEADER;
FILE_DESCRIPTION (('STEP AP214'),
    '1' );
FILE_NAME ('Stand.step',
    '2026-10-24T11:32:06',
    ( '' ),
    ( '' ),
    'SwSTEP 2.0',
    'SolidWorks 2025',
    '' );
FILE_SCHEMA (( 'AUTOMOTIVE_DESIGN' ));
ENDSEC;

DATA;
#61=DIRECTION ( 'NONE',  ( 1.000000000000000000, 0.000000000000000000, 0.000000000000000000 ) ) ;
#76=ORIENTED_EDGE ( 'NONE', *, *, #46509, .T. ) ;
#250=CARTESIAN_POINT ( 'NONE',  ( -0.3937007874015748254, 0.3937007874015748254, -0.7480314960629921295 ) ) ;
#303=ADVANCED_FACE ( 'NONE', ( #34191 ), #6812, .T. ) ;
#339=DIRECTION ( 'NONE',  ( -0.000000000000000000, -0.000000000000000000, 1.000000000000000000 ) ) ;
#551=VECTOR ( 'NONE', #583, 39.37007874015748143 ) ;
#583=DIRECTION ( 'NONE',  ( 0.000000000000000000, 0.000000000000000000, -1.000000000000000000 ) ) ;
#737=MECHANICAL_DESIGN_GEOMETRIC_PRESENTATION_REPRESENTATION('',(#7343),#48493);
#764=EDGE_LOOP ( 'NONE', ( #27424, #28236, #25997, #41547, #30427 ) ) ;
#783=LINE ( 'NONE', #9040, #21665 ) ;
#856=DIRECTION ( 'NONE',  ( 0.7660444431189771253, 0.6427876096865404731, 2.214792131866782686E-16 ) ) ;
#954=ADVANCED_FACE ( 'NONE', ( #44135 ), #4906, .T. ) ;
#1023=VERTEX_POINT ( 'NONE', #37695 ) ;
#1058=DIRECTION ( 'NONE',  ( -1.000000000000000000, 0.000000000000000000, -2.891205793294678326E-16 ) ) ;
#1271=EDGE_CURVE ( 'NONE', #34518, #40355, #50011, .T. ) ;
#1329=VERTEX_POINT ( 'NONE', #4334 ) ;
#1339=VERTEX_POINT ( 'NONE', #23956 ) ;
#1381=ORIENTED_EDGE ( 'NONE', *, *, #45338, .T. ) ;
#1406=LINE ( 'NONE', #1658, #31468 ) ;
#1417=CARTESIAN_POINT ( 'NONE',  ( 0.000000000000000000, 0.3937007874015748254, 0.000000000000000000 ) ) ;
#1451=DIRECTION ( 'NONE',  ( 1.000000000000000000, 0.000000000000000000, 0.000000000000000000 ) ) ;
#1460=LINE ( 'NONE', #32465, #21016 ) ;
#1508=CLOSED_SHELL ( 'NONE', ( #28593, #303, #12996, #41709, #31234, #38345, #40645, #40838, #42452, #45401, #8257, #49683, #4822, #954, #35208, #27540, #18593, #49621, #27006, #21376, #42691, #51026 ) ) ;
#1550=VECTOR ( 'NONE', #16550, 39.37007874015748143 ) ;
#1561=LINE ( 'NONE', #24539, #31653 ) ;
#1658=CARTESIAN_POINT ( 'NONE',  ( -1.377952755905510918, 0.000000000000000000, -4.133858267716536083 ) ) ;
#1700=VECTOR ( 'NONE', #46148, 39.37007874015748854 ) ;
#1701=EDGE_CURVE ( 'NONE', #46418, #14938, #36737, .T. ) ;
#1709=CARTESIAN_POINT ( 'NONE',  ( 0.5905511811023621549, 0.000000000000000000, -4.133858267716536083 ) ) ;
#1811=CARTESIAN_POINT ( 'NONE',  ( 0.8584932060599987924, 0.6447981115998615564, -0.5410498576272521065 ) ) ;
#1880=VECTOR ( 'NONE', #44413, 39.37007874015748143 ) ;
#1971=ORIENTED_EDGE ( 'NONE', *, *, #42708, .F. ) ;
#2299=LINE ( 'NONE', #18301, #1700 ) ;
#2364=LINE ( 'NONE', #6238, #48551 ) ;
#2419=DIRECTION ( 'NONE',  ( -2.214792131866782686E-16, 0.6427876096865404731, 0.7660444431189771253 ) ) ;
#2575=VECTOR ( 'NONE', #25824, 39.37007874015748143 ) ;
#2619=VECTOR ( 'NONE', #14689, 39.37007874015748854 ) ;
#2722=EDGE_CURVE ( 'NONE', #24890, #48785, #11308, .T. ) ;
#2810=CARTESIAN_POINT ( 'NONE',  ( 0.4330136603435741360, 0.5160455853568218787, -0.4330136603435745246 ) ) ;
#2871=CARTESIAN_POINT ( 'NONE',  ( 0.5905511811023621549, 0.000000000000000000, -4.133858267716536083 ) ) ;
#2899=EDGE_CURVE ( 'NONE', #13855, #7934, #28057, .T. ) ;
#2902=CYLINDRICAL_SURFACE ( 'NONE', #50080, 2.854330708661417138 ) ;
#3102=PLANE ( 'NONE',  #41018 ) ;
#3518=EDGE_CURVE ( 'NONE', #13855, #36871, #18683, .T. ) ;
#3599=LINE ( 'NONE', #7979, #16022 ) ;
#3610=FACE_OUTER_BOUND ( 'NONE', #25420, .T. ) ;
#3829=CARTESIAN_POINT ( 'NONE',  ( -2.770917298715281252, 0.6859011407150840123, -3.558318873518431680 ) ) ;
#3841=CARTESIAN_POINT ( 'NONE',  ( -3.346456692913385211, 0.000000000000000000, -4.133858267716536083 ) ) ;
#3894=EDGE_CURVE ( 'NONE', #9591, #32984, #2364, .T. ) ;
#3947=LINE ( 'NONE', #19679, #27733 ) ;
#4173=DIRECTION ( 'NONE',  ( 8.673617379884035472E-17, 0.000000000000000000, 1.000000000000000000 ) ) ;
#4180=ORIENTED_EDGE ( 'NONE', *, *, #45242, .T. ) ;
#4236=EDGE_CURVE ( 'NONE', #20947, #27229, #36396, .T. ) ;
#4271=ORIENTED_EDGE ( 'NONE', *, *, #43186, .T. ) ;
#4334=CARTESIAN_POINT ( 'NONE',  ( 0.3303541855028671037, 0.3937007874015748254, -1.220472440944881942 ) ) ;
#4405=DIRECTION ( 'NONE',  ( -1.000000000000000000, -0.000000000000000000, -1.734839586111147395E-16 ) ) ;
#4582=VERTEX_POINT ( 'NONE', #45269 ) ;
#4670=CARTESIAN_POINT ( 'NONE',  ( -0.7874015748031496509, 1.172985819482486924, -0.9842519685039370358 ) ) ;
#4730=PLANE ( 'NONE',  #44253 ) ;
#4803=CARTESIAN_POINT ( 'NONE',  ( -2.770917298715283028, 0.6859011407150841233, 1.589814936510556720 ) ) ;
#4815=PRODUCT_DEFINITION ( 'UNKNOWN', '', #36630, #34459 ) ;
#4822=ADVANCED_FACE ( 'NONE', ( #34944 ), #34693, .T. ) ;
#4906=PLANE ( 'NONE',  #45958 ) ;
#4921=LINE ( 'NONE', #28919, #44466 ) ;
#4941=ORIENTED_EDGE ( 'NONE', *, *, #19656, .T. ) ;
#5051=UNCERTAINTY_MEASURE_WITH_UNIT (LENGTH_MEASURE( 1.000000000000000082E-05 ), #13245, 'distance_accuracy_value', 'NONE');
#5087=VERTEX_POINT ( 'NONE', #5219 ) ;
#5178=CARTESIAN_POINT ( 'NONE',  ( -1.377952755905513360, 0.000000000000000000, 2.165354330708661568 ) ) ;
#5186=ORIENTED_EDGE ( 'NONE', *, *, #25169, .F. ) ;
#5219=CARTESIAN_POINT ( 'NONE',  ( -1.377952755905510918, 0.000000000000000000, -4.133858267716536083 ) ) ;
#5374=ORIENTED_EDGE ( 'NONE', *, *, #14610, .F. ) ;
#5377=AXIS2_PLACEMENT_3D ( 'NONE', #9544, #17044, #17542 ) ;
#5436=DIRECTION ( 'NONE',  ( 2.891205793294678326E-16, 0.000000000000000000, -1.000000000000000000 ) ) ;
#5556=EDGE_CURVE ( 'NONE', #5087, #40355, #45873, .T. ) ;
#5615=EDGE_CURVE ( 'NONE', #1023, #48695, #35552, .T. ) ;
#5693=CARTESIAN_POINT ( 'NONE',  ( 1.566245445154855531, 1.172985819482486924, -0.9842519685039369248 ) ) ;
#5804=EDGE_LOOP ( 'NONE', ( #24791, #15698, #48121 ) ) ;
#5878=FACE_OUTER_BOUND ( 'NONE', #22395, .T. ) ;
#6164=ORIENTED_EDGE ( 'NONE', *, *, #28622, .T. ) ;
#6221=EDGE_CURVE ( 'NONE', #33190, #13314, #39444, .T. ) ;
#6238=CARTESIAN_POINT ( 'NONE',  ( -1.377952755905513360, 0.000000000000000000, 2.165354330708661568 ) ) ;
#6262=VECTOR ( 'NONE', #1058, 39.37007874015748143 ) ;
#6323=ORIENTED_EDGE ( 'NONE', *, *, #42210, .F. ) ;
#6653=CARTESIAN_POINT ( 'NONE',  ( 1.574803149606300190, 1.172985819482486924, 1.181102362204724532 ) ) ;
#6680=VECTOR ( 'NONE', #39121, 39.37007874015748143 ) ;
#6796=CARTESIAN_POINT ( 'NONE',  ( 0.5905511811023621549, 0.000000000000000000, -1.968503937007874072 ) ) ;
#6812=PLANE ( 'NONE',  #22190 ) ;
#6929=EDGE_CURVE ( 'NONE', #9666, #34518, #27186, .T. ) ;
#7018=( NAMED_UNIT ( * ) SI_UNIT ( $, .STERADIAN. ) SOLID_ANGLE_UNIT ( ) );
#7067=ADVANCED_BREP_SHAPE_REPRESENTATION ( '', ( #40963, #26741 ), #40758 ) ;
#7124=ORIENTED_EDGE ( 'NONE', *, *, #20548, .T. ) ;
#7149=VECTOR ( 'NONE', #24098, 39.37007874015748854 ) ;
#7239=CARTESIAN_POINT ( 'NONE',  ( -3.346456692913385211, 0.000000000000000000, -4.133858267716536083 ) ) ;
#7343=STYLED_ITEM('',(#51080),#40963);
#7494=EDGE_CURVE ( 'NONE', #34034, #46418, #783, .T. ) ;
#7693=ORIENTED_EDGE ( 'NONE', *, *, #14066, .F. ) ;
#7869=CARTESIAN_POINT ( 'NONE',  ( 1.243077785924837197, 0.8677437501918831009, -1.240380476265473098 ) ) ;
#7909=CARTESIAN_POINT ( 'NONE',  ( -3.346456692913385211, 0.000000000000000000, -4.133858267716536083 ) ) ;
#7918=ORIENTED_EDGE ( 'NONE', *, *, #7494, .F. ) ;
#7920=VECTOR ( 'NONE', #25014, 39.37007874015748143 ) ;
#7934=VERTEX_POINT ( 'NONE', #36356 ) ;
#7979=CARTESIAN_POINT ( 'NONE',  ( 0.3303541855028671037, 0.3937007874015748254, 0.000000000000000000 ) ) ;
#8038=LINE ( 'NONE', #27907, #20251 ) ;
#8089=VECTOR ( 'NONE', #22426, 39.37007874015748854 ) ;
#8094=VECTOR ( 'NONE', #8852, 39.37007874015748143 ) ;
#8203=LINE ( 'NONE', #35064, #41288 ) ;
#8257=ADVANCED_FACE ( 'NONE', ( #15826 ), #47031, .T. ) ;
#8281=EDGE_LOOP ( 'NONE', ( #10555, #14334, #1381, #43874 ) ) ;
#8344=DIRECTION ( 'NONE',  ( 0.000000000000000000, 0.000000000000000000, -1.000000000000000000 ) ) ;
#8498=EDGE_CURVE ( 'NONE', #23569, #4582, #10125, .T. ) ;
#8503=VERTEX_POINT ( 'NONE', #38267 ) ;
#8639=ORIENTED_EDGE ( 'NONE', *, *, #48430, .F. ) ;
#8669=UNCERTAINTY_MEASURE_WITH_UNIT (LENGTH_MEASURE( 1.000000000000000082E-05 ), #21318, 'distance_accuracy_value', 'NONE');
#8771=CARTESIAN_POINT ( 'NONE',  ( -0.7874015748031498729, 0.000000000000000000, -1.138269997360109921E-16 ) ) ;
#8801=DIRECTION ( 'NONE',  ( -0.7660444431189771253, 0.6427876096865404731, 0.000000000000000000 ) ) ;
#8852=DIRECTION ( 'NONE',  ( 2.891205793294678326E-16, 0.000000000000000000, -1.000000000000000000 ) ) ;
#8854=AXIS2_PLACEMENT_3D ( 'NONE', #25498, #10517, #17756 ) ;
#8985=EDGE_CURVE ( 'NONE', #7934, #45264, #37307, .T. ) ;
#9006=CARTESIAN_POINT ( 'NONE',  ( -0.3937007874015748254, 3.248031496062991685, -2.362204724409448620 ) ) ;
#9040=CARTESIAN_POINT ( 'NONE',  ( -0.7874015748031495399, 0.000000000000000000, -1.220472440944881942 ) ) ;
#9232=DIRECTION ( 'NONE',  ( 0.000000000000000000, 0.000000000000000000, 1.000000000000000000 ) ) ;
#9385=DIRECTION ( 'NONE',  ( -1.858431260983764056E-16, 0.7660444431189770143, 0.6427876096865403621 ) ) ;
#9467=DIRECTION ( 'NONE',  ( 1.000000000000000000, 0.000000000000000000, 2.775557561562891351E-16 ) ) ;
#9544=CARTESIAN_POINT ( 'NONE',  ( 0.5905511811023627100, 0.000000000000000000, 2.165354330708661568 ) ) ;
#9559=ORIENTED_EDGE ( 'NONE', *, *, #42708, .T. ) ;
#9591=VERTEX_POINT ( 'NONE', #37809 ) ;
#9598=ORIENTED_EDGE ( 'NONE', *, *, #38493, .T. ) ;
#9603=ORIENTED_EDGE ( 'NONE', *, *, #17639, .F. ) ;
#9666=VERTEX_POINT ( 'NONE', #35488 ) ;
#10025=DIRECTION ( 'NONE',  ( 1.000000000000000000, 0.000000000000000000, 0.000000000000000000 ) ) ;
#10085=LINE ( 'NONE', #18086, #2575 ) ;
#10125=LINE ( 'NONE', #26377, #39020 ) ;
#10150=PLANE ( 'NONE',  #12110 ) ;
#10202=ORIENTED_EDGE ( 'NONE', *, *, #30384, .F. ) ;
#10347=DIRECTION ( 'NONE',  ( 0.6427876096865403621, 0.7660444431189770143, 1.858431260983764056E-16 ) ) ;
#10383=SHAPE_REPRESENTATION_RELATIONSHIP ( 'NONE' , 'NONE' ,  #50787, #7067 ) ;
#10387=CARTESIAN_POINT ( 'NONE',  ( 0.5905511811023627100, 0.000000000000000000, 0.000000000000000000 ) ) ;
#10517=DIRECTION ( 'NONE',  ( 0.7660444431189771253, 0.6427876096865404731, -6.644376395600348305E-17 ) ) ;
#10546=CARTESIAN_POINT ( 'NONE',  ( 1.983515723912132378, 0.6859011407150840123, -3.558318873518431236 ) ) ;
#10555=ORIENTED_EDGE ( 'NONE', *, *, #30211, .F. ) ;
#10726=CARTESIAN_POINT ( 'NONE',  ( -1.377952755905512472, 0.000000000000000000, -2.845674993400276405E-16 ) ) ;
#11017=DIRECTION ( 'NONE',  ( 0.6427876096865403621, 0.7660444431189770143, 1.115133390745971592E-16 ) ) ;
#11034=ORIENTED_EDGE ( 'NONE', *, *, #5615, .T. ) ;
#11047=EDGE_LOOP ( 'NONE', ( #27910, #47211, #46524, #34077, #46468 ) ) ;
#11058=DIRECTION ( 'NONE',  ( -1.858431260983764056E-16, 0.7660444431189770143, 0.6427876096865403621 ) ) ;
#11136=VERTEX_POINT ( 'NONE', #6796 ) ;
#11308=LINE ( 'NONE', #22676, #8089 ) ;
#11506=LINE ( 'NONE', #23367, #6680 ) ;
#11522=ORIENTED_EDGE ( 'NONE', *, *, #6221, .T. ) ;
#11528=CARTESIAN_POINT ( 'NONE',  ( 0.4178893628429310447, -0.2057703422145251981, -2.141165755267305126 ) ) ;
#11600=VECTOR ( 'NONE', #13355, 39.37007874015748143 ) ;
#11706=CARTESIAN_POINT ( 'NONE',  ( -0.3937007874015747699, 0.3937007874015748254, -1.220472440944881942 ) ) ;
#11725=LINE ( 'NONE', #10726, #26952 ) ;
#11907=CARTESIAN_POINT ( 'NONE',  ( 0.4330136603435739695, 0.5160455853568215456, -2.362204724409448620 ) ) ;
#11910=LINE ( 'NONE', #23787, #6262 ) ;
#11956=ORIENTED_EDGE ( 'NONE', *, *, #26760, .F. ) ;
#12071=DIRECTION ( 'NONE',  ( -1.734839586111147642E-16, 0.000000000000000000, 1.000000000000000000 ) ) ;
#12110=AXIS2_PLACEMENT_3D ( 'NONE', #22032, #33154, #9385 ) ;
#12140=DIRECTION ( 'NONE',  ( 0.7660444431189771253, 0.6427876096865404731, 2.214792131866782686E-16 ) ) ;
#12162=PLANE ( 'NONE',  #36337 ) ;
#12293=FACE_OUTER_BOUND ( 'NONE', #19503, .T. ) ;
#12335=VERTEX_POINT ( 'NONE', #46024 ) ;
#12449=LINE ( 'NONE', #32343, #16174 ) ;
#12451=LINE ( 'NONE', #24073, #551 ) ;
#12508=EDGE_CURVE ( 'NONE', #5087, #46382, #12449, .T. ) ;
#12520=VECTOR ( 'NONE', #42925, 39.37007874015748143 ) ;
#12543=DIRECTION ( 'NONE',  ( -0.5407162030609375947, -0.6444004775717706579, 0.5407162030609372616 ) ) ;
#12572=EDGE_CURVE ( 'NONE', #14807, #36871, #3947, .T. ) ;
#12804=CARTESIAN_POINT ( 'NONE',  ( -0.7874015748031498729, 0.000000000000000000, -1.138269997360109921E-16 ) ) ;
#12847=EDGE_CURVE ( 'NONE', #31828, #48695, #28123, .T. ) ;
#12938=LINE ( 'NONE', #5178, #1880 ) ;
#12996=ADVANCED_FACE ( 'NONE', ( #21169 ), #16786, .T. ) ;
#13042=EDGE_LOOP ( 'NONE', ( #46697, #42785, #14551, #20817, #23522 ) ) ;
#13063=AXIS2_PLACEMENT_3D ( 'NONE', #28027, #20015, #43763 ) ;
#13096=EDGE_LOOP ( 'NONE', ( #5186, #30353, #11522, #7124 ) ) ;
#13219=EDGE_CURVE ( 'NONE', #14807, #45414, #41462, .T. ) ;
#13245=( CONVERSION_BASED_UNIT ( 'INCH', #13494 ) LENGTH_UNIT ( ) NAMED_UNIT ( #16241 ) );
#13314=VERTEX_POINT ( 'NONE', #1709 ) ;
#13355=DIRECTION ( 'NONE',  ( -3.324886662288880100E-16, 5.168407336632174847E-17, 1.000000000000000000 ) ) ;
#13452=AXIS2_PLACEMENT_3D ( 'NONE', #37308, #49126, #33184 ) ;
#13463=VECTOR ( 'NONE', #23146, 39.37007874015748143 ) ;
#13493=ORIENTED_EDGE ( 'NONE', *, *, #6929, .F. ) ;
#13494=LENGTH_MEASURE_WITH_UNIT ( LENGTH_MEASURE( 0.02539999999999999897 ), #14002 );
#13571=( LENGTH_UNIT ( ) NAMED_UNIT ( * ) SI_UNIT ( $, .METRE. ) );
#13830=DIRECTION ( 'NONE',  ( 0.000000000000000000, 0.000000000000000000, -1.000000000000000000 ) ) ;
#13855=VERTEX_POINT ( 'NONE', #28340 ) ;
#13921=CARTESIAN_POINT ( 'NONE',  ( -1.377952755905510918, 0.000000000000000000, -4.133858267716536083 ) ) ;
#14002=( LENGTH_UNIT ( ) NAMED_UNIT ( * ) SI_UNIT ( $, .METRE. ) );
#14066=EDGE_CURVE ( 'NONE', #45414, #31828, #27002, .T. ) ;
#14105=ORIENTED_EDGE ( 'NONE', *, *, #8985, .F. ) ;
#14281=CARTESIAN_POINT ( 'NONE',  ( -1.377952755905513360, 0.000000000000000000, 2.165354330708661568 ) ) ;
#14334=ORIENTED_EDGE ( 'NONE', *, *, #45825, .F. ) ;
#14444=VECTOR ( 'NONE', #26578, 39.37007874015748854 ) ;
#14551=ORIENTED_EDGE ( 'NONE', *, *, #21861, .T. ) ;
#14555=CARTESIAN_POINT ( 'NONE',  ( 0.4178893628429313778, -0.2057703422145253647, 0.1726618182594314710 ) ) ;
#14610=EDGE_CURVE ( 'NONE', #1329, #50585, #19453, .T. ) ;
#14689=DIRECTION ( 'NONE',  ( 0.5407162030609374836, -0.6444004775717706579, -0.5407162030609372616 ) ) ;
#14748=DIRECTION ( 'NONE',  ( -0.5407162030609373726, -0.6444004775717705469, -0.5407162030609375947 ) ) ;
#14807=VERTEX_POINT ( 'NONE', #36492 ) ;
#14938=VERTEX_POINT ( 'NONE', #25884 ) ;
#15067=CARTESIAN_POINT ( 'NONE',  ( -0.7874015748031498729, 0.000000000000000000, -1.138269997360109921E-16 ) ) ;
#15299=EDGE_CURVE ( 'NONE', #40355, #8503, #43008, .T. ) ;
#15383=EDGE_LOOP ( 'NONE', ( #36199, #50338, #11956, #6323 ) ) ;
#15389=ORIENTED_EDGE ( 'NONE', *, *, #4236, .T. ) ;
#15582=EDGE_LOOP ( 'NONE', ( #9603, #25182, #21470 ) ) ;
#15621=ORIENTED_EDGE ( 'NONE', *, *, #14610, .T. ) ;
#15698=ORIENTED_EDGE ( 'NONE', *, *, #16557, .T. ) ;
#15776=LINE ( 'NONE', #11907, #24591 ) ;
#15785=CARTESIAN_POINT ( 'NONE',  ( -1.377952755905512472, 0.000000000000000000, -2.845674993400276405E-16 ) ) ;
#15825=DIRECTION ( 'NONE',  ( 1.000000000000000000, 0.000000000000000000, 0.000000000000000000 ) ) ;
#15826=FACE_OUTER_BOUND ( 'NONE', #19001, .T. ) ;
#15877=ORIENTED_EDGE ( 'NONE', *, *, #46509, .F. ) ;
#15931=CARTESIAN_POINT ( 'NONE',  ( 0.000000000000000000, 1.172985819482486924, -0.9842519685039369248 ) ) ;
#16022=VECTOR ( 'NONE', #44606, 39.37007874015748143 ) ;
#16174=VECTOR ( 'NONE', #36466, 39.37007874015748143 ) ;
#16202=FACE_OUTER_BOUND ( 'NONE', #17933, .T. ) ;
#16241=DIMENSIONAL_EXPONENTS ( 1.000000000000000000, 0.000000000000000000, 0.000000000000000000, 0.000000000000000000, 0.000000000000000000, 0.000000000000000000, 0.000000000000000000 ) ;
#16250=ORIENTED_EDGE ( 'NONE', *, *, #22026, .T. ) ;
#16272=VECTOR ( 'NONE', #43005, 39.37007874015748854 ) ;
#16347=CARTESIAN_POINT ( 'NONE',  ( -0.7874015748031498729, 0.000000000000000000, -1.138269997360109921E-16 ) ) ;
#16398=DIRECTION ( 'NONE',  ( 1.000000000000000000, 0.000000000000000000, 0.000000000000000000 ) ) ;
#16488=ORIENTED_EDGE ( 'NONE', *, *, #13219, .T. ) ;
#16535=DIRECTION ( 'NONE',  ( 0.6427876096865403621, -0.7660444431189770143, 1.858431260983764056E-16 ) ) ;
#16550=DIRECTION ( 'NONE',  ( 1.000000000000000000, -0.000000000000000000, 2.891205793294678326E-16 ) ) ;
#16557=EDGE_CURVE ( 'NONE', #46515, #36309, #35624, .T. ) ;
#16786=PLANE ( 'NONE',  #5377 ) ;
#16800=EDGE_LOOP ( 'NONE', ( #43859, #43943, #32468 ) ) ;
#16805=PLANE ( 'NONE',  #22484 ) ;
#16809=FACE_OUTER_BOUND ( 'NONE', #13096, .T. ) ;
#17044=DIRECTION ( 'NONE',  ( 0.000000000000000000, 0.6427876096865404731, 0.7660444431189771253 ) ) ;
#17232=LINE ( 'NONE', #48669, #11600 ) ;
#17542=DIRECTION ( 'NONE',  ( 0.000000000000000000, -0.7660444431189770143, 0.6427876096865403621 ) ) ;
#17548=VECTOR ( 'NONE', #5436, 39.37007874015748143 ) ;
#17561=CARTESIAN_POINT ( 'NONE',  ( 0.4330136603435741360, 0.5160455853568218787, -0.4330136603435745246 ) ) ;
#17587=DIRECTION ( 'NONE',  ( -4.336808689942018969E-17, -5.168407336632174847E-17, -1.000000000000000000 ) ) ;
#17614=ORIENTED_EDGE ( 'NONE', *, *, #28629, .F. ) ;
#17639=EDGE_CURVE ( 'NONE', #13314, #40666, #1460, .T. ) ;
#17724=APPLICATION_CONTEXT ( 'automotive_design' ) ;
#17749=FACE_OUTER_BOUND ( 'NONE', #764, .T. ) ;
#17756=DIRECTION ( 'NONE',  ( -0.6427876096865403621, 0.7660444431189770143, 0.000000000000000000 ) ) ;
#17770=LINE ( 'NONE', #41271, #44870 ) ;
#17897=ORIENTED_EDGE ( 'NONE', *, *, #12572, .F. ) ;
#17933=EDGE_LOOP ( 'NONE', ( #49101, #49208, #25356, #23548 ) ) ;
#17978=EDGE_CURVE ( 'NONE', #7934, #24890, #32016, .T. ) ;
#18086=CARTESIAN_POINT ( 'NONE',  ( 1.983515723912132822, 0.6859011407150841233, 1.589814936510557386 ) ) ;
#18254=DIRECTION ( 'NONE',  ( 0.000000000000000000, 0.7660444431189770143, 0.6427876096865403621 ) ) ;
#18261=PLANE ( 'NONE',  #8854 ) ;
#18301=CARTESIAN_POINT ( 'NONE',  ( -0.7874015748031498729, 0.000000000000000000, -1.138269997360109921E-16 ) ) ;
#18302=CARTESIAN_POINT ( 'NONE',  ( 0.000000000000000000, 0.000000000000000000, -1.968503937007874072 ) ) ;
#18340=CARTESIAN_POINT ( 'NONE',  ( -1.220415235146723454, 0.5160455853568216567, -1.535490276664301046 ) ) ;
#18482=ORIENTED_EDGE ( 'NONE', *, *, #37087, .T. ) ;
#18593=ADVANCED_FACE ( 'NONE', ( #30430 ), #45890, .T. ) ;
#18683=LINE ( 'NONE', #14555, #43564 ) ;
#18817=LINE ( 'NONE', #34566, #2619 ) ;
#18842=CARTESIAN_POINT ( 'NONE',  ( -1.205290937646080307, -0.2057703422145251981, -2.141165755267305126 ) ) ;
#19001=EDGE_LOOP ( 'NONE', ( #36905, #15621, #10202, #7918 ) ) ;
#19270=EDGE_CURVE ( 'NONE', #4582, #12335, #48356, .T. ) ;
#19387=FACE_OUTER_BOUND ( 'NONE', #5804, .T. ) ;
#19453=LINE ( 'NONE', #27454, #7149 ) ;
#19503=EDGE_LOOP ( 'NONE', ( #1971, #30394, #27280, #5374, #35932, #7693, #26067, #26048 ) ) ;
#19593=DIRECTION ( 'NONE',  ( 0.000000000000000000, 0.7660444431189770143, 0.6427876096865403621 ) ) ;
#19656=EDGE_CURVE ( 'NONE', #50585, #48785, #12451, .T. ) ;
#19679=CARTESIAN_POINT ( 'NONE',  ( 0.000000000000000000, 0.000000000000000000, 0.000000000000000000 ) ) ;
#19797=ORIENTED_EDGE ( 'NONE', *, *, #23166, .T. ) ;
#20015=DIRECTION ( 'NONE',  ( -0.7660444431189771253, 0.6427876096865404731, 0.000000000000000000 ) ) ;
#20101=FACE_OUTER_BOUND ( 'NONE', #15582, .T. ) ;
#20206=CYLINDRICAL_SURFACE ( 'NONE', #25899, 2.854330708661417138 ) ;
#20251=VECTOR ( 'NONE', #36438, 39.37007874015748143 ) ;
#20318=ORIENTED_EDGE ( 'NONE', *, *, #6929, .T. ) ;
#20319=DIRECTION ( 'NONE',  ( -1.000000000000000000, 0.000000000000000000, -0.000000000000000000 ) ) ;
#20352=APPLICATION_CONTEXT ( 'automotive_design' ) ;
#20360=CARTESIAN_POINT ( 'NONE',  ( -1.377952755905513360, 0.000000000000000000, 2.165354330708661568 ) ) ;
#20381=ORIENTED_EDGE ( 'NONE', *, *, #5556, .F. ) ;
#20415=CARTESIAN_POINT ( 'NONE',  ( 0.5905511811023621549, 0.000000000000000000, -4.133858267716536083 ) ) ;
#20467=DIRECTION ( 'NONE',  ( 0.000000000000000000, 0.000000000000000000, 1.000000000000000000 ) ) ;
#20548=EDGE_CURVE ( 'NONE', #13314, #11136, #33038, .T. ) ;
#20659=VECTOR ( 'NONE', #35301, 39.37007874015748143 ) ;
#20731=PRODUCT_DEFINITION_SHAPE ( 'NONE', 'NONE',  #4815 ) ;
#20817=ORIENTED_EDGE ( 'NONE', *, *, #12572, .T. ) ;
#20930=LINE ( 'NONE', #32049, #17548 ) ;
#20947=VERTEX_POINT ( 'NONE', #12804 ) ;
#20984=CARTESIAN_POINT ( 'NONE',  ( 0.000000000000000000, 0.000000000000000000, 0.000000000000000000 ) ) ;
#21016=VECTOR ( 'NONE', #9467, 39.37007874015748143 ) ;
#21169=FACE_OUTER_BOUND ( 'NONE', #16800, .T. ) ;
#21318=( CONVERSION_BASED_UNIT ( 'INCH', #44785 ) LENGTH_UNIT ( ) NAMED_UNIT ( #48537 ) );
#21376=ADVANCED_FACE ( 'NONE', ( #35714 ), #4730, .T. ) ;
#21470=ORIENTED_EDGE ( 'NONE', *, *, #47915, .T. ) ;
#21507=DIRECTION ( 'NONE',  ( 0.000000000000000000, -1.000000000000000000, 0.000000000000000000 ) ) ;
#21665=VECTOR ( 'NONE', #16535, 39.37007874015748854 ) ;
#21675=CARTESIAN_POINT ( 'NONE',  ( -1.377952755905511362, 0.000000000000000000, -1.968503937007874516 ) ) ;
#21861=EDGE_CURVE ( 'NONE', #45264, #14807, #1561, .T. ) ;
#22026=EDGE_CURVE ( 'NONE', #9591, #8503, #40178, .T. ) ;
#22032=CARTESIAN_POINT ( 'NONE',  ( -0.7874015748031493178, 0.000000000000000000, -1.968503937007874072 ) ) ;
#22059=PLANE ( 'NONE',  #13452 ) ;
#22093=VECTOR ( 'NONE', #31349, 39.37007874015748854 ) ;
#22190=AXIS2_PLACEMENT_3D ( 'NONE', #49875, #49378, #33183 ) ;
#22395=EDGE_LOOP ( 'NONE', ( #33866, #30477, #9598, #48179, #34265 ) ) ;
#22426=DIRECTION ( 'NONE',  ( -0.5407162030609373726, -0.6444004775717706579, -0.5407162030609373726 ) ) ;
#22445=ORIENTED_EDGE ( 'NONE', *, *, #1701, .F. ) ;
#22484=AXIS2_PLACEMENT_3D ( 'NONE', #36686, #48509, #25311 ) ;
#22676=CARTESIAN_POINT ( 'NONE',  ( 0.5755393941981044037, 0.6859011407150840123, -1.392964542809770334 ) ) ;
#22787=CARTESIAN_POINT ( 'NONE',  ( -1.117755760306016644, 0.3937007874015748254, -1.220472440944882164 ) ) ;
#22878=VECTOR ( 'NONE', #17587, 39.37007874015748143 ) ;
#22881=ORIENTED_EDGE ( 'NONE', *, *, #27201, .T. ) ;
#22930=AXIS2_PLACEMENT_3D ( 'NONE', #32898, #21507, #29763 ) ;
#22977=DIRECTION ( 'NONE',  ( -0.7660444431189771253, 0.6427876096865404731, -2.879229771426817147E-16 ) ) ;
#23146=DIRECTION ( 'NONE',  ( -3.758567531283081874E-16, 0.000000000000000000, 1.000000000000000000 ) ) ;
#23166=EDGE_CURVE ( 'NONE', #9666, #46382, #46176, .T. ) ;
#23177=PLANE ( 'NONE',  #25578 ) ;
#23367=CARTESIAN_POINT ( 'NONE',  ( -0.3937007874015747699, 0.3937007874015748254, -1.220472440944881942 ) ) ;
#23522=ORIENTED_EDGE ( 'NONE', *, *, #3518, .F. ) ;
#23530=LINE ( 'NONE', #27914, #25339 ) ;
#23548=ORIENTED_EDGE ( 'NONE', *, *, #5615, .F. ) ;
#23569=VERTEX_POINT ( 'NONE', #6653 ) ;
#23787=CARTESIAN_POINT ( 'NONE',  ( -0.7874015748031493178, 0.000000000000000000, -1.968503937007874072 ) ) ;
#23829=ORIENTED_EDGE ( 'NONE', *, *, #48430, .T. ) ;
#23956=CARTESIAN_POINT ( 'NONE',  ( -1.220415235146723676, 0.5160455853568218787, -0.4330136603435745246 ) ) ;
#23971=CARTESIAN_POINT ( 'NONE',  ( 0.4330136603435738585, 0.5160455853568214346, -1.535490276664301046 ) ) ;
#23990=EDGE_CURVE ( 'NONE', #13855, #23569, #8038, .T. ) ;
#24030=EDGE_CURVE ( 'NONE', #14938, #46382, #11910, .T. ) ;
#24073=CARTESIAN_POINT ( 'NONE',  ( 0.000000000000000000, 0.000000000000000000, 0.000000000000000000 ) ) ;
#24089=DIRECTION ( 'NONE',  ( -1.000000000000000000, 0.000000000000000000, -0.000000000000000000 ) ) ;
#24098=DIRECTION ( 'NONE',  ( -0.6427876096865403621, -0.7660444431189770143, 0.000000000000000000 ) ) ;
#24391=EDGE_CURVE ( 'NONE', #36871, #4582, #40737, .T. ) ;
#24526=CARTESIAN_POINT ( 'NONE',  ( -0.7874015748031495399, 0.000000000000000000, -1.220472440944881942 ) ) ;
#24539=CARTESIAN_POINT ( 'NONE',  ( 0.000000000000000000, 0.000000000000000000, 0.000000000000000000 ) ) ;
#24591=VECTOR ( 'NONE', #39531, 39.37007874015748143 ) ;
#24791=ORIENTED_EDGE ( 'NONE', *, *, #42108, .T. ) ;
#24822=ORIENTED_EDGE ( 'NONE', *, *, #26760, .T. ) ;
#24890=VERTEX_POINT ( 'NONE', #23971 ) ;
#25014=DIRECTION ( 'NONE',  ( 0.000000000000000000, 0.000000000000000000, 1.000000000000000000 ) ) ;
#25169=EDGE_CURVE ( 'NONE', #13855, #11136, #46860, .T. ) ;
#25175=VECTOR ( 'NONE', #43361, 39.37007874015748143 ) ;
#25182=ORIENTED_EDGE ( 'NONE', *, *, #6221, .F. ) ;
#25192=CARTESIAN_POINT ( 'NONE',  ( -1.220415235146723454, 0.5160455853568218787, -2.362204724409449064 ) ) ;
#25242=CARTESIAN_POINT ( 'NONE',  ( 0.000000000000000000, 0.000000000000000000, -1.968503937007874072 ) ) ;
#25311=DIRECTION ( 'NONE',  ( 0.000000000000000000, -0.7660444431189770143, 0.6427876096865403621 ) ) ;
#25339=VECTOR ( 'NONE', #4173, 39.37007874015748143 ) ;
#25356=ORIENTED_EDGE ( 'NONE', *, *, #12847, .T. ) ;
#25420=EDGE_LOOP ( 'NONE', ( #20318, #39884, #43926, #44303, #39788 ) ) ;
#25491=PLANE ( 'NONE',  #33713 ) ;
#25498=CARTESIAN_POINT ( 'NONE',  ( 2.559055118110236560, 0.000000000000000000, -4.133858267716535195 ) ) ;
#25578=AXIS2_PLACEMENT_3D ( 'NONE', #43555, #12071, #31960 ) ;
#25642=FACE_OUTER_BOUND ( 'NONE', #44374, .T. ) ;
#25782=EDGE_LOOP ( 'NONE', ( #33495, #4180, #6164, #11034, #44985, #36800, #31492, #15877 ) ) ;
#25824=DIRECTION ( 'NONE',  ( 0.5407162030609374836, -0.6444004775717706579, 0.5407162030609373726 ) ) ;
#25862=ORIENTED_EDGE ( 'NONE', *, *, #15299, .F. ) ;
#25884=CARTESIAN_POINT ( 'NONE',  ( -0.7874015748031493178, 0.000000000000000000, -1.968503937007874072 ) ) ;
#25899=AXIS2_PLACEMENT_3D ( 'NONE', #32105, #339, #15825 ) ;
#25997=ORIENTED_EDGE ( 'NONE', *, *, #25169, .T. ) ;
#26048=ORIENTED_EDGE ( 'NONE', *, *, #21861, .F. ) ;
#26067=ORIENTED_EDGE ( 'NONE', *, *, #13219, .F. ) ;
#26164=DIRECTION ( 'NONE',  ( -1.858431260983764056E-16, -0.7660444431189770143, 0.6427876096865403621 ) ) ;
#26181=PLANE ( 'NONE',  #36524 ) ;
#26282=VECTOR ( 'NONE', #1451, 39.37007874015748143 ) ;
#26377=CARTESIAN_POINT ( 'NONE',  ( 0.5905511811023627100, 0.000000000000000000, 2.165354330708661568 ) ) ;
#26536=DIRECTION ( 'NONE',  ( 0.5407162030609373726, -0.6444004775717706579, -0.5407162030609372616 ) ) ;
#26578=DIRECTION ( 'NONE',  ( 0.5407162030609374836, -0.6444004775717706579, -0.5407162030609372616 ) ) ;
#26727=CARTESIAN_POINT ( 'NONE',  ( 0.8584932060599983483, 0.6447981115998610013, -1.427454079380622742 ) ) ;
#26741=AXIS2_PLACEMENT_3D ( 'NONE', #20984, #20467, #36229 ) ;
#26760=EDGE_CURVE ( 'NONE', #27229, #32984, #11725, .T. ) ;
#26936=VECTOR ( 'NONE', #16398, 39.37007874015748143 ) ;
#26952=VECTOR ( 'NONE', #42207, 39.37007874015748143 ) ;
#27002=LINE ( 'NONE', #46355, #41750 ) ;
#27006=ADVANCED_FACE ( 'NONE', ( #25642 ), #10150, .T. ) ;
#27070=EDGE_CURVE ( 'NONE', #1339, #36309, #39998, .T. ) ;
#27186=LINE ( 'NONE', #47022, #12520 ) ;
#27201=EDGE_CURVE ( 'NONE', #40666, #12335, #23530, .T. ) ;
#27229=VERTEX_POINT ( 'NONE', #15785 ) ;
#27280=ORIENTED_EDGE ( 'NONE', *, *, #19656, .F. ) ;
#27386=EDGE_CURVE ( 'NONE', #13855, #33190, #33856, .T. ) ;
#27424=ORIENTED_EDGE ( 'NONE', *, *, #17978, .F. ) ;
#27454=CARTESIAN_POINT ( 'NONE',  ( 0.000000000000000000, 0.000000000000000000, -1.220472440944881942 ) ) ;
#27540=ADVANCED_FACE ( 'NONE', ( #3610 ), #3102, .T. ) ;
#27733=VECTOR ( 'NONE', #61, 39.37007874015748143 ) ;
#27884=PRODUCT_CONTEXT ( 'NONE', #17724, 'mechanical' ) ;
#27907=CARTESIAN_POINT ( 'NONE',  ( 1.574803149606299746, 1.172985819482486702, -1.033098100527919830E-16 ) ) ;
#27910=ORIENTED_EDGE ( 'NONE', *, *, #45242, .F. ) ;
#27914=CARTESIAN_POINT ( 'NONE',  ( 2.559055118110236560, 0.000000000000000000, -4.133858267716535195 ) ) ;
#28027=CARTESIAN_POINT ( 'NONE',  ( 0.000000000000000000, 0.000000000000000000, 0.000000000000000000 ) ) ;
#28057=LINE ( 'NONE', #15931, #42726 ) ;
#28093=VECTOR ( 'NONE', #14748, 39.37007874015748143 ) ;
#28123=LINE ( 'NONE', #250, #25175 ) ;
#28236=ORIENTED_EDGE ( 'NONE', *, *, #2899, .F. ) ;
#28340=CARTESIAN_POINT ( 'NONE',  ( 1.574803149606299524, 1.172985819482486924, -0.9842519685039369248 ) ) ;
#28409=DIRECTION ( 'NONE',  ( -0.6427876096865403621, -0.7660444431189770143, 0.000000000000000000 ) ) ;
#28593=ADVANCED_FACE ( 'NONE', ( #47994 ), #16805, .T. ) ;
#28622=EDGE_CURVE ( 'NONE', #20947, #1023, #20930, .T. ) ;
#28629=EDGE_CURVE ( 'NONE', #32984, #8503, #12938, .T. ) ;
#28658=VECTOR ( 'NONE', #30446, 39.37007874015748143 ) ;
#28838=VECTOR ( 'NONE', #32536, 39.37007874015748143 ) ;
#28870=DIRECTION ( 'NONE',  ( -0.000000000000000000, -0.000000000000000000, 1.000000000000000000 ) ) ;
#28919=CARTESIAN_POINT ( 'NONE',  ( -0.3937007874015748254, 0.000000000000000000, -0.7480314960629921295 ) ) ;
#29029=DIRECTION ( 'NONE',  ( 0.000000000000000000, -1.000000000000000000, 0.000000000000000000 ) ) ;
#29070=VECTOR ( 'NONE', #26536, 39.37007874015748854 ) ;
#29171=DIRECTION ( 'NONE',  ( -0.5407162030609373726, -0.6444004775717706579, 0.5407162030609373726 ) ) ;
#29178=LINE ( 'NONE', #4670, #1550 ) ;
#29399=LINE ( 'NONE', #10546, #29070 ) ;
#29493=( NAMED_UNIT ( * ) SI_UNIT ( $, .STERADIAN. ) SOLID_ANGLE_UNIT ( ) );
#29763=DIRECTION ( 'NONE',  ( 0.000000000000000000, -0.000000000000000000, -1.000000000000000000 ) ) ;
#29803=DIRECTION ( 'NONE',  ( -1.858431260983764056E-16, -0.7660444431189770143, 0.6427876096865403621 ) ) ;
#29810=EDGE_LOOP ( 'NONE', ( #39139, #9559, #14105 ) ) ;
#30211=EDGE_CURVE ( 'NONE', #1329, #31828, #3599, .T. ) ;
#30288=PLANE ( 'NONE',  #39425 ) ;
#30353=ORIENTED_EDGE ( 'NONE', *, *, #27386, .T. ) ;
#30384=EDGE_CURVE ( 'NONE', #46418, #50585, #17770, .T. ) ;
#30394=ORIENTED_EDGE ( 'NONE', *, *, #2722, .T. ) ;
#30427=ORIENTED_EDGE ( 'NONE', *, *, #2722, .F. ) ;
#30430=FACE_OUTER_BOUND ( 'NONE', #50990, .T. ) ;
#30446=DIRECTION ( 'NONE',  ( -0.5407162030609373726, -0.6444004775717707689, -0.5407162030609374836 ) ) ;
#30477=ORIENTED_EDGE ( 'NONE', *, *, #23990, .T. ) ;
#30592=LINE ( 'NONE', #30842, #22093 ) ;
#30842=CARTESIAN_POINT ( 'NONE',  ( -1.205290937646081417, -0.2057703422145253647, 0.1726618182594312212 ) ) ;
#30978=CARTESIAN_POINT ( 'NONE',  ( 0.5905511811023621549, 0.000000000000000000, -4.133858267716536083 ) ) ;
#31174=CARTESIAN_POINT ( 'NONE',  ( -1.377952755905510918, 0.000000000000000000, -4.133858267716536083 ) ) ;
#31234=ADVANCED_FACE ( 'NONE', ( #20101 ), #34850, .T. ) ;
#31349=DIRECTION ( 'NONE',  ( 0.5407162030609372616, -0.6444004775717706579, 0.5407162030609374836 ) ) ;
#31350=ORIENTED_EDGE ( 'NONE', *, *, #41127, .T. ) ;
#31468=VECTOR ( 'NONE', #33172, 39.37007874015748143 ) ;
#31492=ORIENTED_EDGE ( 'NONE', *, *, #1701, .T. ) ;
#31647=CARTESIAN_POINT ( 'NONE',  ( 0.000000000000000000, 0.000000000000000000, -1.220472440944881942 ) ) ;
#31653=VECTOR ( 'NONE', #29171, 39.37007874015748854 ) ;
#31679=CARTESIAN_POINT ( 'NONE',  ( -0.7874015748031497619, 6.389997247649651107E-17, -0.7480314960629921295 ) ) ;
#31776=SHAPE_DEFINITION_REPRESENTATION ( #20731, #50787 ) ;
#31828=VERTEX_POINT ( 'NONE', #36584 ) ;
#31946=DIRECTION ( 'NONE',  ( -0.6427876096865403621, 0.7660444431189770143, -7.432978702377923406E-17 ) ) ;
#31960=DIRECTION ( 'NONE',  ( 1.000000000000000000, 0.000000000000000000, 1.734839586111147642E-16 ) ) ;
#32016=( BOUNDED_CURVE ( )  B_SPLINE_CURVE ( 3, ( #38862, #7869, #26727, #42474 ),
 .UNSPECIFIED., .F., .F. ) 
 B_SPLINE_CURVE_WITH_KNOTS ( ( 4, 4 ),
 ( 2.384712079142225161, 2.847747046894732126 ),
 .UNSPECIFIED. ) 
 CURVE ( )  GEOMETRIC_REPRESENTATION_ITEM ( )  RATIONAL_B_SPLINE_CURVE ( ( 1.000000000000000000, 0.9822128812423629451, 0.9822128812423629451, 1.000000000000000000 ) ) 
 REPRESENTATION_ITEM ( '' )  );
#32049=CARTESIAN_POINT ( 'NONE',  ( -0.7874015748031498729, 0.000000000000000000, -1.138269997360109921E-16 ) ) ;
#32105=CARTESIAN_POINT ( 'NONE',  ( -0.3937007874015748254, 3.248031496062991685, -2.362204724409448620 ) ) ;
#32194=ORIENTED_EDGE ( 'NONE', *, *, #24391, .T. ) ;
#32282=DIRECTION ( 'NONE',  ( 0.6427876096865403621, -0.7660444431189770143, 1.858431260983764056E-16 ) ) ;
#32343=CARTESIAN_POINT ( 'NONE',  ( -1.377952755905510918, 0.000000000000000000, -4.133858267716536083 ) ) ;
#32465=CARTESIAN_POINT ( 'NONE',  ( 0.5905511811023621549, 0.000000000000000000, -4.133858267716536083 ) ) ;
#32468=ORIENTED_EDGE ( 'NONE', *, *, #8498, .T. ) ;
#32536=DIRECTION ( 'NONE',  ( -1.000000000000000000, 0.000000000000000000, -2.891205793294678326E-16 ) ) ;
#32898=CARTESIAN_POINT ( 'NONE',  ( 0.000000000000000000, 0.000000000000000000, 0.000000000000000000 ) ) ;
#32929=CARTESIAN_POINT ( 'NONE',  ( 0.5905511811023627100, 0.000000000000000000, 2.165354330708661568 ) ) ;
#32948=EDGE_LOOP ( 'NONE', ( #16488, #18482, #50164, #15389, #24822, #38325, #25862, #20381, #49863, #41842, #22445, #35557, #4941, #4271, #43803, #34113, #22881, #37734, #33359, #17897 ) ) ;
#32984=VERTEX_POINT ( 'NONE', #20360 ) ;
#33038=LINE ( 'NONE', #44617, #7920 ) ;
#33154=DIRECTION ( 'NONE',  ( 2.214792131866782686E-16, 0.6427876096865404731, -0.7660444431189771253 ) ) ;
#33172=DIRECTION ( 'NONE',  ( 0.5407162030609374836, -0.6444004775717705469, -0.5407162030609374836 ) ) ;
#33183=DIRECTION ( 'NONE',  ( -0.6427876096865403621, -0.7660444431189770143, 0.000000000000000000 ) ) ;
#33184=DIRECTION ( 'NONE',  ( 0.6427876096865403621, -0.7660444431189770143, 1.858431260983764056E-16 ) ) ;
#33190=VERTEX_POINT ( 'NONE', #45866 ) ;
#33359=ORIENTED_EDGE ( 'NONE', *, *, #24391, .F. ) ;
#33403=PLANE ( 'NONE',  #22930 ) ;
#33495=ORIENTED_EDGE ( 'NONE', *, *, #42108, .F. ) ;
#33516=DIRECTION ( 'NONE',  ( 0.000000000000000000, 0.6427876096865404731, -0.7660444431189771253 ) ) ;
#33651=FACE_OUTER_BOUND ( 'NONE', #32948, .T. ) ;
#33713=AXIS2_PLACEMENT_3D ( 'NONE', #25242, #33516, #18254 ) ;
#33735=DIRECTION ( 'NONE',  ( 0.000000000000000000, 0.000000000000000000, -1.000000000000000000 ) ) ;
#33856=LINE ( 'NONE', #41588, #22878 ) ;
#33866=ORIENTED_EDGE ( 'NONE', *, *, #27386, .F. ) ;
#33921=ORIENTED_EDGE ( 'NONE', *, *, #3894, .F. ) ;
#34004=ORIENTED_EDGE ( 'NONE', *, *, #1271, .F. ) ;
#34034=VERTEX_POINT ( 'NONE', #22787 ) ;
#34077=ORIENTED_EDGE ( 'NONE', *, *, #42210, .T. ) ;
#34113=ORIENTED_EDGE ( 'NONE', *, *, #17639, .T. ) ;
#34163=CARTESIAN_POINT ( 'NONE',  ( -1.645894780863148332, 0.6447981115998611124, -0.5410498576272523286 ) ) ;
#34168=VECTOR ( 'NONE', #12543, 39.37007874015748854 ) ;
#34191=FACE_OUTER_BOUND ( 'NONE', #48470, .T. ) ;
#34265=ORIENTED_EDGE ( 'NONE', *, *, #47915, .F. ) ;
#34398=( NAMED_UNIT ( * ) PLANE_ANGLE_UNIT ( ) SI_UNIT ( $, .RADIAN. ) );
#34439=VECTOR ( 'NONE', #13830, 39.37007874015748143 ) ;
#34459=PRODUCT_DEFINITION_CONTEXT ( 'detailed design', #20352, 'design' ) ;
#34518=VERTEX_POINT ( 'NONE', #39676 ) ;
#34556=EDGE_LOOP ( 'NONE', ( #17614, #33921, #16250 ) ) ;
#34566=CARTESIAN_POINT ( 'NONE',  ( -1.362940969001253944, 0.6859011407150840123, -1.392964542809770556 ) ) ;
#34678=VECTOR ( 'NONE', #31946, 39.37007874015748854 ) ;
#34680=ORIENTED_EDGE ( 'NONE', *, *, #23990, .F. ) ;
#34693=PLANE ( 'NONE',  #45916 ) ;
#34850=PLANE ( 'NONE',  #38262 ) ;
#34944=FACE_OUTER_BOUND ( 'NONE', #11047, .T. ) ;
#35064=CARTESIAN_POINT ( 'NONE',  ( -1.117755760306017088, 0.3937007874015748254, -2.093391932325144326E-16 ) ) ;
#35208=ADVANCED_FACE ( 'NONE', ( #38791 ), #30288, .T. ) ;
#35301=DIRECTION ( 'NONE',  ( -1.000000000000000000, 0.000000000000000000, -1.156482317317869599E-17 ) ) ;
#35488=CARTESIAN_POINT ( 'NONE',  ( -2.362204724409449508, 1.172985819482486924, -0.9842519685039374799 ) ) ;
#35552=LINE ( 'NONE', #31679, #34678 ) ;
#35557=ORIENTED_EDGE ( 'NONE', *, *, #30384, .T. ) ;
#35624=( BOUNDED_CURVE ( )  B_SPLINE_CURVE ( 3, ( #18340, #46184, #50285, #42588 ),
 .UNSPECIFIED., .F., .F. ) 
 B_SPLINE_CURVE_WITH_KNOTS ( ( 4, 4 ),
 ( 3.435438260284853662, 3.898473228037360627 ),
 .UNSPECIFIED. ) 
 CURVE ( )  GEOMETRIC_REPRESENTATION_ITEM ( )  RATIONAL_B_SPLINE_CURVE ( ( 1.000000000000000000, 0.9822128812423629451, 0.9822128812423629451, 1.000000000000000000 ) ) 
 REPRESENTATION_ITEM ( '' )  );
#35636=CARTESIAN_POINT ( 'NONE',  ( -1.377952755905512472, 0.000000000000000000, -2.845674993400276405E-16 ) ) ;
#35714=FACE_OUTER_BOUND ( 'NONE', #25782, .T. ) ;
#35847=ORIENTED_EDGE ( 'NONE', *, *, #12508, .F. ) ;
#35932=ORIENTED_EDGE ( 'NONE', *, *, #30211, .T. ) ;
#36199=ORIENTED_EDGE ( 'NONE', *, *, #45555, .T. ) ;
#36224=ORIENTED_EDGE ( 'NONE', *, *, #5556, .T. ) ;
#36229=DIRECTION ( 'NONE',  ( 1.000000000000000000, 0.000000000000000000, 0.000000000000000000 ) ) ;
#36309=VERTEX_POINT ( 'NONE', #49111 ) ;
#36337=AXIS2_PLACEMENT_3D ( 'NONE', #20415, #8801, #28409 ) ;
#36356=CARTESIAN_POINT ( 'NONE',  ( 1.566245445154855531, 1.172985819482486924, -0.9842519685039369248 ) ) ;
#36396=LINE ( 'NONE', #8771, #28838 ) ;
#36438=DIRECTION ( 'NONE',  ( 4.336808689942019585E-17, 5.168407336632174847E-17, 1.000000000000000000 ) ) ;
#36466=DIRECTION ( 'NONE',  ( -2.891205793294678326E-16, 0.000000000000000000, 1.000000000000000000 ) ) ;
#36492=CARTESIAN_POINT ( 'NONE',  ( 0.000000000000000000, 0.000000000000000000, 0.000000000000000000 ) ) ;
#36524=AXIS2_PLACEMENT_3D ( 'NONE', #1417, #29029, #44768 ) ;
#36584=CARTESIAN_POINT ( 'NONE',  ( 0.3303541855028670482, 0.3937007874015748254, -0.7480314960629920185 ) ) ;
#36630=PRODUCT_DEFINITION_FORMATION_WITH_SPECIFIED_SOURCE ( 'ANY', '', #50723, .NOT_KNOWN. ) ;
#36686=CARTESIAN_POINT ( 'NONE',  ( 0.000000000000000000, 0.000000000000000000, 0.000000000000000000 ) ) ;
#36737=LINE ( 'NONE', #16347, #8094 ) ;
#36745=VECTOR ( 'NONE', #33735, 39.37007874015748143 ) ;
#36800=ORIENTED_EDGE ( 'NONE', *, *, #7494, .T. ) ;
#36831=LINE ( 'NONE', #43781, #26282 ) ;
#36835=CARTESIAN_POINT ( 'NONE',  ( 0.000000000000000000, 0.000000000000000000, 0.000000000000000000 ) ) ;
#36871=VERTEX_POINT ( 'NONE', #10387 ) ;
#36905=ORIENTED_EDGE ( 'NONE', *, *, #45825, .T. ) ;
#37051=FACE_OUTER_BOUND ( 'NONE', #46823, .T. ) ;
#37087=EDGE_CURVE ( 'NONE', #45414, #1023, #4921, .T. ) ;
#37194=CARTESIAN_POINT ( 'NONE',  ( 1.243077785924837197, 0.8677437501918831009, -0.7281234607424009742 ) ) ;
#37307=( BOUNDED_CURVE ( )  B_SPLINE_CURVE ( 3, ( #5693, #37194, #1811, #17561 ),
 .UNSPECIFIED., .F., .F. ) 
 B_SPLINE_CURVE_WITH_KNOTS ( ( 4, 4 ),
 ( 5.526304732732018721, 5.989339700484524798 ),
 .UNSPECIFIED. ) 
 CURVE ( )  GEOMETRIC_REPRESENTATION_ITEM ( )  RATIONAL_B_SPLINE_CURVE ( ( 1.000000000000000000, 0.9822128812423631672, 0.9822128812423631672, 1.000000000000000000 ) ) 
 REPRESENTATION_ITEM ( '' )  );
#37308=CARTESIAN_POINT ( 'NONE',  ( -1.377952755905510918, 0.000000000000000000, -4.133858267716536083 ) ) ;
#37695=CARTESIAN_POINT ( 'NONE',  ( -0.7874015748031496509, 0.000000000000000000, -0.7480314960629921295 ) ) ;
#37734=ORIENTED_EDGE ( 'NONE', *, *, #19270, .F. ) ;
#37741=DIRECTION ( 'NONE',  ( 0.5407162030609372616, -0.6444004775717706579, 0.5407162030609374836 ) ) ;
#37809=CARTESIAN_POINT ( 'NONE',  ( -2.362204724409450396, 1.172985819482486924, 1.181102362204724088 ) ) ;
#37848=LINE ( 'NONE', #25192, #34439 ) ;
#38262=AXIS2_PLACEMENT_3D ( 'NONE', #30978, #47439, #19593 ) ;
#38267=CARTESIAN_POINT ( 'NONE',  ( -3.346456692913387432, 0.000000000000000000, 2.165354330708661124 ) ) ;
#38325=ORIENTED_EDGE ( 'NONE', *, *, #28629, .T. ) ;
#38345=ADVANCED_FACE ( 'NONE', ( #16809 ), #12162, .T. ) ;
#38493=EDGE_CURVE ( 'NONE', #23569, #12335, #10085, .T. ) ;
#38785=CARTESIAN_POINT ( 'NONE',  ( -2.030479360727987181, 0.8677437501918839891, -0.7281234607424019734 ) ) ;
#38791=FACE_OUTER_BOUND ( 'NONE', #34556, .T. ) ;
#38862=CARTESIAN_POINT ( 'NONE',  ( 1.566245445154855531, 1.172985819482486924, -0.9842519685039369248 ) ) ;
#39020=VECTOR ( 'NONE', #42123, 39.37007874015748854 ) ;
#39121=DIRECTION ( 'NONE',  ( 1.000000000000000000, 0.000000000000000000, 0.000000000000000000 ) ) ;
#39139=ORIENTED_EDGE ( 'NONE', *, *, #17978, .T. ) ;
#39400=CARTESIAN_POINT ( 'NONE',  ( 2.559055118110236560, 0.000000000000000000, -4.133858267716535195 ) ) ;
#39425=AXIS2_PLACEMENT_3D ( 'NONE', #14281, #2419, #26164 ) ;
#39444=LINE ( 'NONE', #2871, #28093 ) ;
#39531=DIRECTION ( 'NONE',  ( -0.000000000000000000, -0.000000000000000000, 1.000000000000000000 ) ) ;
#39676=CARTESIAN_POINT ( 'NONE',  ( -2.362204724409448620, 1.172985819482487146, -3.149606299212598604 ) ) ;
#39788=ORIENTED_EDGE ( 'NONE', *, *, #45555, .F. ) ;
#39884=ORIENTED_EDGE ( 'NONE', *, *, #1271, .T. ) ;
#39998=( BOUNDED_CURVE ( )  B_SPLINE_CURVE ( 3, ( #41902, #34163, #38785, #49849 ),
 .UNSPECIFIED., .F., .F. ) 
 B_SPLINE_CURVE_WITH_KNOTS ( ( 4, 4 ),
 ( 0.2938456066950616563, 0.7568805744475686215 ),
 .UNSPECIFIED. ) 
 CURVE ( )  GEOMETRIC_REPRESENTATION_ITEM ( )  RATIONAL_B_SPLINE_CURVE ( ( 1.000000000000000000, 0.9822128812423629451, 0.9822128812423629451, 1.000000000000000000 ) ) 
 REPRESENTATION_ITEM ( '' )  );
#40175=PLANE ( 'NONE',  #13063 ) ;
#40178=LINE ( 'NONE', #4803, #34168 ) ;
#40355=VERTEX_POINT ( 'NONE', #3841 ) ;
#40439=AXIS2_PLACEMENT_3D ( 'NONE', #11706, #8344, #24089 ) ;
#40645=ADVANCED_FACE ( 'NONE', ( #17749 ), #25491, .T. ) ;
#40666=VERTEX_POINT ( 'NONE', #39400 ) ;
#40737=LINE ( 'NONE', #41748, #48300 ) ;
#40756=DIRECTION ( 'NONE',  ( 1.000000000000000000, 0.000000000000000000, 0.000000000000000000 ) ) ;
#40758=( GEOMETRIC_REPRESENTATION_CONTEXT ( 3 ) GLOBAL_UNCERTAINTY_ASSIGNED_CONTEXT ( ( #5051 ) ) GLOBAL_UNIT_ASSIGNED_CONTEXT ( ( #13245, #44966, #29493 ) ) REPRESENTATION_CONTEXT ( 'NONE', 'WORKASPACE' ) );
#40838=ADVANCED_FACE ( 'NONE', ( #12293 ), #40175, .T. ) ;
#40963=MANIFOLD_SOLID_BREP ( 'Cut-Extrude1', #1508 ) ;
#41018=AXIS2_PLACEMENT_3D ( 'NONE', #7239, #22977, #10347 ) ;
#41127=EDGE_CURVE ( 'NONE', #9666, #36309, #29178, .T. ) ;
#41271=CARTESIAN_POINT ( 'NONE',  ( -0.3937007874015747699, 0.000000000000000000, -1.220472440944881942 ) ) ;
#41288=VECTOR ( 'NONE', #42796, 39.37007874015748143 ) ;
#41462=LINE ( 'NONE', #36835, #36745 ) ;
#41547=ORIENTED_EDGE ( 'NONE', *, *, #43186, .F. ) ;
#41588=CARTESIAN_POINT ( 'NONE',  ( 1.574803149606299080, 1.172985819482486924, -4.133858267716535195 ) ) ;
#41667=DIRECTION ( 'NONE',  ( -0.5407162030609373726, -0.6444004775717706579, 0.5407162030609373726 ) ) ;
#41709=ADVANCED_FACE ( 'NONE', ( #5878 ), #18261, .T. ) ;
#41748=CARTESIAN_POINT ( 'NONE',  ( 0.5905511811023627100, 0.000000000000000000, 0.000000000000000000 ) ) ;
#41750=VECTOR ( 'NONE', #11017, 39.37007874015748854 ) ;
#41842=ORIENTED_EDGE ( 'NONE', *, *, #24030, .F. ) ;
#41902=CARTESIAN_POINT ( 'NONE',  ( -1.220415235146723676, 0.5160455853568218787, -0.4330136603435745246 ) ) ;
#42108=EDGE_CURVE ( 'NONE', #1339, #46515, #37848, .T. ) ;
#42123=DIRECTION ( 'NONE',  ( -0.5407162030609373726, -0.6444004775717706579, 0.5407162030609373726 ) ) ;
#42207=DIRECTION ( 'NONE',  ( -2.891205793294678326E-16, 0.000000000000000000, 1.000000000000000000 ) ) ;
#42210=EDGE_CURVE ( 'NONE', #9666, #27229, #30592, .T. ) ;
#42452=ADVANCED_FACE ( 'NONE', ( #33651 ), #33403, .T. ) ;
#42474=CARTESIAN_POINT ( 'NONE',  ( 0.4330136603435738585, 0.5160455853568214346, -1.535490276664301046 ) ) ;
#42588=CARTESIAN_POINT ( 'NONE',  ( -2.353647019958005071, 1.172985819482486924, -0.9842519685039374799 ) ) ;
#42691=ADVANCED_FACE ( 'NONE', ( #19387 ), #2902, .F. ) ;
#42708=EDGE_CURVE ( 'NONE', #24890, #45264, #15776, .T. ) ;
#42726=VECTOR ( 'NONE', #20319, 39.37007874015748143 ) ;
#42785=ORIENTED_EDGE ( 'NONE', *, *, #8985, .T. ) ;
#42796=DIRECTION ( 'NONE',  ( -2.891205793294678326E-16, 0.000000000000000000, 1.000000000000000000 ) ) ;
#42925=DIRECTION ( 'NONE',  ( 3.324886662288880100E-16, -5.168407336632174847E-17, -1.000000000000000000 ) ) ;
#42927=ORIENTED_EDGE ( 'NONE', *, *, #8498, .F. ) ;
#43005=DIRECTION ( 'NONE',  ( -0.5407162030609373726, -0.6444004775717706579, -0.5407162030609373726 ) ) ;
#43008=LINE ( 'NONE', #7909, #13463 ) ;
#43186=EDGE_CURVE ( 'NONE', #48785, #11136, #36831, .T. ) ;
#43361=DIRECTION ( 'NONE',  ( -1.000000000000000000, -0.000000000000000000, -1.734839586111147395E-16 ) ) ;
#43555=CARTESIAN_POINT ( 'NONE',  ( -0.3937007874015748254, 0.3937007874015748254, -0.7480314960629921295 ) ) ;
#43564=VECTOR ( 'NONE', #41667, 39.37007874015748854 ) ;
#43672=CARTESIAN_POINT ( 'NONE',  ( -1.117755760306016644, 0.3937007874015748254, -0.7480314960629922405 ) ) ;
#43763=DIRECTION ( 'NONE',  ( -0.6427876096865403621, -0.7660444431189770143, 0.000000000000000000 ) ) ;
#43781=CARTESIAN_POINT ( 'NONE',  ( 0.000000000000000000, 0.000000000000000000, -1.968503937007874072 ) ) ;
#43803=ORIENTED_EDGE ( 'NONE', *, *, #20548, .F. ) ;
#43859=ORIENTED_EDGE ( 'NONE', *, *, #19270, .T. ) ;
#43874=ORIENTED_EDGE ( 'NONE', *, *, #12847, .F. ) ;
#43926=ORIENTED_EDGE ( 'NONE', *, *, #15299, .T. ) ;
#43943=ORIENTED_EDGE ( 'NONE', *, *, #38493, .F. ) ;
#44135=FACE_OUTER_BOUND ( 'NONE', #15383, .T. ) ;
#44212=FACE_OUTER_BOUND ( 'NONE', #29810, .T. ) ;
#44253=AXIS2_PLACEMENT_3D ( 'NONE', #47545, #856, #48312 ) ;
#44303=ORIENTED_EDGE ( 'NONE', *, *, #22026, .F. ) ;
#44374=EDGE_LOOP ( 'NONE', ( #48490, #76, #45380, #44603, #31350 ) ) ;
#44413=DIRECTION ( 'NONE',  ( -1.000000000000000000, 0.000000000000000000, -2.891205793294678326E-16 ) ) ;
#44466=VECTOR ( 'NONE', #4405, 39.37007874015748143 ) ;
#44603=ORIENTED_EDGE ( 'NONE', *, *, #23166, .F. ) ;
#44606=DIRECTION ( 'NONE',  ( 0.000000000000000000, 0.000000000000000000, 1.000000000000000000 ) ) ;
#44617=CARTESIAN_POINT ( 'NONE',  ( 0.5905511811023621549, 0.000000000000000000, -4.133858267716536083 ) ) ;
#44768=DIRECTION ( 'NONE',  ( 0.000000000000000000, -0.000000000000000000, -1.000000000000000000 ) ) ;
#44785=LENGTH_MEASURE_WITH_UNIT ( LENGTH_MEASURE( 0.02539999999999999897 ), #13571 );
#44870=VECTOR ( 'NONE', #10025, 39.37007874015748143 ) ;
#44966=( NAMED_UNIT ( * ) PLANE_ANGLE_UNIT ( ) SI_UNIT ( $, .RADIAN. ) );
#44984=AXIS2_PLACEMENT_3D ( 'NONE', #13921, #46144, #11058 ) ;
#44985=ORIENTED_EDGE ( 'NONE', *, *, #45338, .F. ) ;
#45242=EDGE_CURVE ( 'NONE', #1339, #20947, #2299, .T. ) ;
#45264=VERTEX_POINT ( 'NONE', #2810 ) ;
#45269=CARTESIAN_POINT ( 'NONE',  ( 0.5905511811023627100, 0.000000000000000000, 2.165354330708661568 ) ) ;
#45338=EDGE_CURVE ( 'NONE', #34034, #48695, #8203, .T. ) ;
#45380=ORIENTED_EDGE ( 'NONE', *, *, #24030, .T. ) ;
#45401=ADVANCED_FACE ( 'NONE', ( #16202 ), #23177, .T. ) ;
#45414=VERTEX_POINT ( 'NONE', #50739 ) ;
#45555=EDGE_CURVE ( 'NONE', #9666, #9591, #17232, .T. ) ;
#45825=EDGE_CURVE ( 'NONE', #34034, #1329, #11506, .T. ) ;
#45866=CARTESIAN_POINT ( 'NONE',  ( 1.574803149606299524, 1.172985819482487146, -3.149606299212598159 ) ) ;
#45873=LINE ( 'NONE', #31174, #20659 ) ;
#45890=PLANE ( 'NONE',  #44984 ) ;
#45916=AXIS2_PLACEMENT_3D ( 'NONE', #15067, #50624, #29803 ) ;
#45958=AXIS2_PLACEMENT_3D ( 'NONE', #35636, #12140, #32282 ) ;
#46024=CARTESIAN_POINT ( 'NONE',  ( 2.559055118110237004, 0.000000000000000000, 2.165354330708661568 ) ) ;
#46144=DIRECTION ( 'NONE',  ( 8.859168527467109606E-18, 0.6427876096865404731, -0.7660444431189771253 ) ) ;
#46148=DIRECTION ( 'NONE',  ( 0.5407162030609372616, -0.6444004775717706579, 0.5407162030609374836 ) ) ;
#46176=LINE ( 'NONE', #18842, #14444 ) ;
#46184=CARTESIAN_POINT ( 'NONE',  ( -1.645894780863147000, 0.6447981115998608903, -1.427454079380623408 ) ) ;
#46355=CARTESIAN_POINT ( 'NONE',  ( 5.361844333726674129E-17, 6.389997247649651107E-17, -0.7480314960629920185 ) ) ;
#46382=VERTEX_POINT ( 'NONE', #21675 ) ;
#46418=VERTEX_POINT ( 'NONE', #24526 ) ;
#46468=ORIENTED_EDGE ( 'NONE', *, *, #4236, .F. ) ;
#46509=EDGE_CURVE ( 'NONE', #46515, #14938, #18817, .T. ) ;
#46515=VERTEX_POINT ( 'NONE', #50253 ) ;
#46524=ORIENTED_EDGE ( 'NONE', *, *, #41127, .F. ) ;
#46697=ORIENTED_EDGE ( 'NONE', *, *, #2899, .T. ) ;
#46823=EDGE_LOOP ( 'NONE', ( #19797, #35847, #8639, #13493 ) ) ;
#46860=LINE ( 'NONE', #11528, #16272 ) ;
#47022=CARTESIAN_POINT ( 'NONE',  ( -2.362204724409447731, 1.172985819482486924, -4.133858267716536083 ) ) ;
#47031=PLANE ( 'NONE',  #40439 ) ;
#47211=ORIENTED_EDGE ( 'NONE', *, *, #27070, .T. ) ;
#47439=DIRECTION ( 'NONE',  ( 2.126200446592111359E-16, 0.6427876096865404731, -0.7660444431189771253 ) ) ;
#47545=CARTESIAN_POINT ( 'NONE',  ( -0.7874015748031498729, 0.000000000000000000, -1.138269997360109921E-16 ) ) ;
#47590=ORIENTED_EDGE ( 'NONE', *, *, #3518, .T. ) ;
#47915=EDGE_CURVE ( 'NONE', #33190, #40666, #29399, .T. ) ;
#47994=FACE_OUTER_BOUND ( 'NONE', #13042, .T. ) ;
#48121=ORIENTED_EDGE ( 'NONE', *, *, #27070, .F. ) ;
#48179=ORIENTED_EDGE ( 'NONE', *, *, #27201, .F. ) ;
#48300=VECTOR ( 'NONE', #9232, 39.37007874015748143 ) ;
#48312=DIRECTION ( 'NONE',  ( 0.6427876096865403621, -0.7660444431189770143, 1.858431260983764056E-16 ) ) ;
#48356=LINE ( 'NONE', #32929, #26936 ) ;
#48430=EDGE_CURVE ( 'NONE', #34518, #5087, #1406, .T. ) ;
#48470=EDGE_LOOP ( 'NONE', ( #34680, #47590, #32194, #42927 ) ) ;
#48490=ORIENTED_EDGE ( 'NONE', *, *, #16557, .F. ) ;
#48493=( GEOMETRIC_REPRESENTATION_CONTEXT ( 3 ) GLOBAL_UNCERTAINTY_ASSIGNED_CONTEXT ( ( #8669 ) ) GLOBAL_UNIT_ASSIGNED_CONTEXT ( ( #21318, #34398, #7018 ) ) REPRESENTATION_CONTEXT ( 'NONE', 'WORKASPACE' ) );
#48509=DIRECTION ( 'NONE',  ( 0.000000000000000000, 0.6427876096865404731, 0.7660444431189771253 ) ) ;
#48537=DIMENSIONAL_EXPONENTS ( 1.000000000000000000, 0.000000000000000000, 0.000000000000000000, 0.000000000000000000, 0.000000000000000000, 0.000000000000000000, 0.000000000000000000 ) ;
#48551=VECTOR ( 'NONE', #37741, 39.37007874015748854 ) ;
#48669=CARTESIAN_POINT ( 'NONE',  ( -2.362204724409449952, 1.172985819482486702, -6.724448087328469681E-16 ) ) ;
#48695=VERTEX_POINT ( 'NONE', #43672 ) ;
#48785=VERTEX_POINT ( 'NONE', #18302 ) ;
#49101=ORIENTED_EDGE ( 'NONE', *, *, #37087, .F. ) ;
#49111=CARTESIAN_POINT ( 'NONE',  ( -2.353647019958005071, 1.172985819482486924, -0.9842519685039374799 ) ) ;
#49126=DIRECTION ( 'NONE',  ( 0.7660444431189771253, 0.6427876096865404731, 2.214792131866782686E-16 ) ) ;
#49208=ORIENTED_EDGE ( 'NONE', *, *, #14066, .T. ) ;
#49378=DIRECTION ( 'NONE',  ( -0.7660444431189771253, 0.6427876096865404731, 0.000000000000000000 ) ) ;
#49379=FACE_OUTER_BOUND ( 'NONE', #8281, .T. ) ;
#49621=ADVANCED_FACE ( 'NONE', ( #37051 ), #22059, .T. ) ;
#49683=ADVANCED_FACE ( 'NONE', ( #49379 ), #26181, .F. ) ;
#49849=CARTESIAN_POINT ( 'NONE',  ( -2.353647019958005071, 1.172985819482486924, -0.9842519685039374799 ) ) ;
#49863=ORIENTED_EDGE ( 'NONE', *, *, #12508, .T. ) ;
#49875=CARTESIAN_POINT ( 'NONE',  ( 0.5905511811023627100, 0.000000000000000000, 0.000000000000000000 ) ) ;
#50011=LINE ( 'NONE', #3829, #28658 ) ;
#50080=AXIS2_PLACEMENT_3D ( 'NONE', #9006, #28870, #40756 ) ;
#50164=ORIENTED_EDGE ( 'NONE', *, *, #28622, .F. ) ;
#50253=CARTESIAN_POINT ( 'NONE',  ( -1.220415235146723454, 0.5160455853568216567, -1.535490276664301046 ) ) ;
#50285=CARTESIAN_POINT ( 'NONE',  ( -2.030479360727985849, 0.8677437501918828788, -1.240380476265474208 ) ) ;
#50338=ORIENTED_EDGE ( 'NONE', *, *, #3894, .T. ) ;
#50585=VERTEX_POINT ( 'NONE', #31647 ) ;
#50624=DIRECTION ( 'NONE',  ( -2.214792131866782686E-16, 0.6427876096865404731, 0.7660444431189771253 ) ) ;
#50723=PRODUCT ( 'Stand', 'Stand', '', ( #27884 ) ) ;
#50739=CARTESIAN_POINT ( 'NONE',  ( 0.000000000000000000, 0.000000000000000000, -0.7480314960629920185 ) ) ;
#50787=SHAPE_REPRESENTATION ( 'Stand', ( #26741 ), #40758 ) ;
#50990=EDGE_LOOP ( 'NONE', ( #36224, #34004, #23829 ) ) ;
#51026=ADVANCED_FACE ( 'NONE', ( #44212 ), #20206, .F. ) ;
#51074=COLOUR_RGB('Sky Blue',0.24,0.69,0.87);
#51075=FILL_AREA_STYLE_COLOUR('',#51074);
#51076=FILL_AREA_STYLE('',(#51075));
#51077=SURFACE_STYLE_FILL_AREA(#51076);
#51078=SURFACE_SIDE_STYLE('',(#51077));
#51079=SURFACE_STYLE_USAGE(.BOTH.,#51078);
#51080=PRESENTATION_STYLE_ASSIGNMENT((#51079));
ENDSEC;
END-ISO-10303-21;
